ISO-10303-21;
HEADER;
/* Generated by software containing ST-Developer
 * from STEP Tools, Inc. (www.steptools.com) 
 */

FILE_DESCRIPTION(
/* description */ ('STEP AP214'),
/* implementation_level */ '2;1');

FILE_NAME(
/* name */ 'Hex Screw Grade AB ISO.step',
/* time_stamp */ '2026-11-14T04:35:10-08:00',
/* author */ (''),
/* organization */ (''),
/* preprocessor_version */ 'ST-DEVELOPER v20.2',
/* originating_system */ 'Autodesk Translation Framework v15.17.0.0',
/* authorisation */ '');

FILE_SCHEMA (('AUTOMOTIVE_DESIGN { 1 0 10303 214 3 1 1 }'));
ENDSEC;

DATA;
#10=MECHANICAL_DESIGN_GEOMETRIC_PRESENTATION_REPRESENTATION('',(#110),#2477);
#27=(
BOUNDED_CURVE()
B_SPLINE_CURVE(2,(#2404,#2405,#2406),.UNSPECIFIED.,.F.,.F.)
B_SPLINE_CURVE_WITH_KNOTS((3,3),(-3.12660138416105,-1.84743207297635),
 .UNSPECIFIED.)
CURVE()
GEOMETRIC_REPRESENTATION_ITEM()
RATIONAL_B_SPLINE_CURVE((1.7511213796222,1.7511213796222,1.62539652116965))
REPRESENTATION_ITEM('')
);
#28=(
BOUNDED_CURVE()
B_SPLINE_CURVE(2,(#2407,#2408,#2409),.UNSPECIFIED.,.F.,.F.)
B_SPLINE_CURVE_WITH_KNOTS((3,3),(-4.40577069534575,-3.12660138416105),
 .UNSPECIFIED.)
CURVE()
GEOMETRIC_REPRESENTATION_ITEM()
RATIONAL_B_SPLINE_CURVE((1.62539652116964,1.75112137962219,1.75112137962219))
REPRESENTATION_ITEM('')
);
#29=(
BOUNDED_CURVE()
B_SPLINE_CURVE(2,(#2412,#2413,#2414),.UNSPECIFIED.,.F.,.F.)
B_SPLINE_CURVE_WITH_KNOTS((3,3),(-3.12660138416105,-1.84743207297636),
 .UNSPECIFIED.)
CURVE()
GEOMETRIC_REPRESENTATION_ITEM()
RATIONAL_B_SPLINE_CURVE((1.75112137962219,1.75112137962219,1.62539652116965))
REPRESENTATION_ITEM('')
);
#30=(
BOUNDED_CURVE()
B_SPLINE_CURVE(2,(#2415,#2416,#2417),.UNSPECIFIED.,.F.,.F.)
B_SPLINE_CURVE_WITH_KNOTS((3,3),(-4.40577069534575,-3.12660138416105),
 .UNSPECIFIED.)
CURVE()
GEOMETRIC_REPRESENTATION_ITEM()
RATIONAL_B_SPLINE_CURVE((1.62539652116965,1.7511213796222,1.7511213796222))
REPRESENTATION_ITEM('')
);
#31=(
BOUNDED_CURVE()
B_SPLINE_CURVE(2,(#2420,#2421,#2422),.UNSPECIFIED.,.F.,.F.)
B_SPLINE_CURVE_WITH_KNOTS((3,3),(-4.40577069534574,-3.12660138416105),
 .UNSPECIFIED.)
CURVE()
GEOMETRIC_REPRESENTATION_ITEM()
RATIONAL_B_SPLINE_CURVE((1.62539652116965,1.7511213796222,1.7511213796222))
REPRESENTATION_ITEM('')
);
#32=(
BOUNDED_CURVE()
B_SPLINE_CURVE(2,(#2423,#2424,#2425),.UNSPECIFIED.,.F.,.F.)
B_SPLINE_CURVE_WITH_KNOTS((3,3),(-3.12660138416105,-1.84743207297636),
 .UNSPECIFIED.)
CURVE()
GEOMETRIC_REPRESENTATION_ITEM()
RATIONAL_B_SPLINE_CURVE((1.75112137962219,1.75112137962219,1.62539652116965))
REPRESENTATION_ITEM('')
);
#33=(
BOUNDED_CURVE()
B_SPLINE_CURVE(2,(#2428,#2429,#2430),.UNSPECIFIED.,.F.,.F.)
B_SPLINE_CURVE_WITH_KNOTS((3,3),(-4.40577069534576,-3.12660138416105),
 .UNSPECIFIED.)
CURVE()
GEOMETRIC_REPRESENTATION_ITEM()
RATIONAL_B_SPLINE_CURVE((1.62539652116965,1.7511213796222,1.7511213796222))
REPRESENTATION_ITEM('')
);
#34=(
BOUNDED_CURVE()
B_SPLINE_CURVE(2,(#2431,#2432,#2433),.UNSPECIFIED.,.F.,.F.)
B_SPLINE_CURVE_WITH_KNOTS((3,3),(-3.12660138416105,-1.84743207297636),
 .UNSPECIFIED.)
CURVE()
GEOMETRIC_REPRESENTATION_ITEM()
RATIONAL_B_SPLINE_CURVE((1.75112137962219,1.75112137962219,1.62539652116965))
REPRESENTATION_ITEM('')
);
#35=(
BOUNDED_CURVE()
B_SPLINE_CURVE(2,(#2436,#2437,#2438),.UNSPECIFIED.,.F.,.F.)
B_SPLINE_CURVE_WITH_KNOTS((3,3),(-3.12660138416105,-1.84743207297636),
 .UNSPECIFIED.)
CURVE()
GEOMETRIC_REPRESENTATION_ITEM()
RATIONAL_B_SPLINE_CURVE((1.75112137962219,1.75112137962219,1.62539652116965))
REPRESENTATION_ITEM('')
);
#36=(
BOUNDED_CURVE()
B_SPLINE_CURVE(2,(#2439,#2440,#2441),.UNSPECIFIED.,.F.,.F.)
B_SPLINE_CURVE_WITH_KNOTS((3,3),(-4.40577069534574,-3.12660138416105),
 .UNSPECIFIED.)
CURVE()
GEOMETRIC_REPRESENTATION_ITEM()
RATIONAL_B_SPLINE_CURVE((1.62539652116965,1.75112137962219,1.75112137962219))
REPRESENTATION_ITEM('')
);
#37=(
BOUNDED_CURVE()
B_SPLINE_CURVE(2,(#2444,#2445,#2446),.UNSPECIFIED.,.F.,.F.)
B_SPLINE_CURVE_WITH_KNOTS((3,3),(-4.40577069534575,-3.12660138416105),
 .UNSPECIFIED.)
CURVE()
GEOMETRIC_REPRESENTATION_ITEM()
RATIONAL_B_SPLINE_CURVE((1.62539652116965,1.75112137962219,1.75112137962219))
REPRESENTATION_ITEM('')
);
#38=(
BOUNDED_CURVE()
B_SPLINE_CURVE(2,(#2447,#2448,#2449),.UNSPECIFIED.,.F.,.F.)
B_SPLINE_CURVE_WITH_KNOTS((3,3),(-3.12660138416105,-1.84743207297636),
 .UNSPECIFIED.)
CURVE()
GEOMETRIC_REPRESENTATION_ITEM()
RATIONAL_B_SPLINE_CURVE((1.75112137962219,1.75112137962219,1.62539652116964))
REPRESENTATION_ITEM('')
);
#39=CONICAL_SURFACE('',#1565,7.33266666666667,0.785398163397449);
#40=CONICAL_SURFACE('',#1584,12.75,1.0471975511966);
#41=CONICAL_SURFACE('',#1585,12.75,1.0471975511966);
#42=CONICAL_SURFACE('',#1586,12.75,1.0471975511966);
#43=CONICAL_SURFACE('',#1587,12.75,1.0471975511966);
#44=CONICAL_SURFACE('',#1588,12.75,1.0471975511966);
#45=CONICAL_SURFACE('',#1589,12.75,1.0471975511966);
#46=TOROIDAL_SURFACE('',#1552,9.06666666666667,0.566666666666667);
#49=FACE_BOUND('',#255,.T.);
#67=CIRCLE('',#1553,8.5);
#68=CIRCLE('',#1554,8.5);
#69=CIRCLE('',#1555,0.566666666666667);
#70=CIRCLE('',#1556,9.06666666666667);
#71=CIRCLE('',#1558,12.75);
#72=CIRCLE('',#1559,12.75);
#73=CIRCLE('',#1560,12.75);
#74=CIRCLE('',#1561,12.75);
#75=CIRCLE('',#1562,12.75);
#76=CIRCLE('',#1563,12.75);
#77=CIRCLE('',#1564,12.75);
#78=CIRCLE('',#1566,8.5);
#79=CIRCLE('',#1567,7.33266666666667);
#80=CIRCLE('',#1578,12.75);
#81=CIRCLE('',#1579,12.75);
#82=CIRCLE('',#1580,12.75);
#83=CIRCLE('',#1581,12.75);
#84=CIRCLE('',#1582,12.75);
#85=CIRCLE('',#1583,12.75);
#97=CYLINDRICAL_SURFACE('',#1557,12.75);
#98=CYLINDRICAL_SURFACE('',#1568,8.5);
#102=SHAPE_REPRESENTATION_RELATIONSHIP('SRR','None',#2500,#106);
#106=ADVANCED_BREP_SHAPE_REPRESENTATION('',(#114),#2476);
#110=STYLED_ITEM('',(#2529),#114);
#114=MANIFOLD_SOLID_BREP('Body1',#1430);
#169=FACE_OUTER_BOUND('',#250,.T.);
#170=FACE_OUTER_BOUND('',#251,.T.);
#171=FACE_OUTER_BOUND('',#252,.T.);
#172=FACE_OUTER_BOUND('',#253,.T.);
#173=FACE_OUTER_BOUND('',#254,.T.);
#174=FACE_OUTER_BOUND('',#256,.T.);
#175=FACE_OUTER_BOUND('',#257,.T.);
#176=FACE_OUTER_BOUND('',#258,.T.);
#177=FACE_OUTER_BOUND('',#259,.T.);
#178=FACE_OUTER_BOUND('',#260,.T.);
#179=FACE_OUTER_BOUND('',#261,.T.);
#180=FACE_OUTER_BOUND('',#262,.T.);
#181=FACE_OUTER_BOUND('',#263,.T.);
#182=FACE_OUTER_BOUND('',#264,.T.);
#183=FACE_OUTER_BOUND('',#265,.T.);
#184=FACE_OUTER_BOUND('',#266,.T.);
#185=FACE_OUTER_BOUND('',#267,.T.);
#186=FACE_OUTER_BOUND('',#268,.T.);
#187=FACE_OUTER_BOUND('',#269,.T.);
#188=FACE_OUTER_BOUND('',#270,.T.);
#189=FACE_OUTER_BOUND('',#271,.T.);
#190=FACE_OUTER_BOUND('',#272,.T.);
#191=FACE_OUTER_BOUND('',#273,.T.);
#192=FACE_OUTER_BOUND('',#274,.T.);
#193=FACE_OUTER_BOUND('',#275,.T.);
#250=EDGE_LOOP('',(#1184,#1185,#1186,#1187,#1188));
#251=EDGE_LOOP('',(#1189,#1190,#1191,#1192,#1193,#1194,#1195,#1196,#1197));
#252=EDGE_LOOP('',(#1198,#1199,#1200,#1201));
#253=EDGE_LOOP('',(#1202,#1203,#1204,#1205,#1206));
#254=EDGE_LOOP('',(#1207));
#255=EDGE_LOOP('',(#1208));
#256=EDGE_LOOP('',(#1209));
#257=EDGE_LOOP('',(#1210,#1211,#1212));
#258=EDGE_LOOP('',(#1213,#1214,#1215));
#259=EDGE_LOOP('',(#1216,#1217,#1218));
#260=EDGE_LOOP('',(#1219,#1220,#1221));
#261=EDGE_LOOP('',(#1222,#1223,#1224));
#262=EDGE_LOOP('',(#1225,#1226,#1227));
#263=EDGE_LOOP('',(#1228,#1229,#1230,#1231,#1232,#1233));
#264=EDGE_LOOP('',(#1234,#1235,#1236));
#265=EDGE_LOOP('',(#1237,#1238,#1239));
#266=EDGE_LOOP('',(#1240,#1241,#1242));
#267=EDGE_LOOP('',(#1243,#1244,#1245));
#268=EDGE_LOOP('',(#1246,#1247,#1248));
#269=EDGE_LOOP('',(#1249,#1250,#1251));
#270=EDGE_LOOP('',(#1252,#1253,#1254,#1255,#1256,#1257));
#271=EDGE_LOOP('',(#1258,#1259,#1260,#1261,#1262,#1263));
#272=EDGE_LOOP('',(#1264,#1265,#1266,#1267,#1268,#1269));
#273=EDGE_LOOP('',(#1270,#1271,#1272,#1273,#1274,#1275));
#274=EDGE_LOOP('',(#1276,#1277,#1278,#1279,#1280,#1281));
#275=EDGE_LOOP('',(#1282,#1283,#1284,#1285,#1286,#1287));
#402=LINE('',#2348,#549);
#403=LINE('',#2359,#550);
#404=LINE('',#2362,#551);
#405=LINE('',#2367,#552);
#406=LINE('',#2368,#553);
#407=LINE('',#2371,#554);
#408=LINE('',#2372,#555);
#409=LINE('',#2375,#556);
#410=LINE('',#2376,#557);
#411=LINE('',#2379,#558);
#412=LINE('',#2380,#559);
#413=LINE('',#2383,#560);
#414=LINE('',#2384,#561);
#415=LINE('',#2387,#562);
#416=LINE('',#2388,#563);
#417=LINE('',#2451,#564);
#418=LINE('',#2452,#565);
#419=LINE('',#2454,#566);
#420=LINE('',#2456,#567);
#421=LINE('',#2458,#568);
#422=LINE('',#2460,#569);
#549=VECTOR('',#1896,12.75);
#550=VECTOR('',#1909,7.33266666666667);
#551=VECTOR('',#1914,8.5);
#552=VECTOR('',#1921,1000.);
#553=VECTOR('',#1922,1000.);
#554=VECTOR('',#1925,1000.);
#555=VECTOR('',#1926,1000.);
#556=VECTOR('',#1929,1000.);
#557=VECTOR('',#1930,1000.);
#558=VECTOR('',#1933,1000.);
#559=VECTOR('',#1934,1000.);
#560=VECTOR('',#1937,1000.);
#561=VECTOR('',#1938,1000.);
#562=VECTOR('',#1941,1000.);
#563=VECTOR('',#1942,1000.);
#564=VECTOR('',#1971,1000.);
#565=VECTOR('',#1972,1000.);
#566=VECTOR('',#1975,1000.);
#567=VECTOR('',#1978,1000.);
#568=VECTOR('',#1981,1000.);
#569=VECTOR('',#1984,1000.);
#667=VERTEX_POINT('',#2332);
#668=VERTEX_POINT('',#2333);
#669=VERTEX_POINT('',#2336);
#670=VERTEX_POINT('',#2340);
#671=VERTEX_POINT('',#2341);
#672=VERTEX_POINT('',#2343);
#673=VERTEX_POINT('',#2345);
#674=VERTEX_POINT('',#2347);
#675=VERTEX_POINT('',#2350);
#676=VERTEX_POINT('',#2352);
#677=VERTEX_POINT('',#2356);
#678=VERTEX_POINT('',#2358);
#679=VERTEX_POINT('',#2366);
#680=VERTEX_POINT('',#2370);
#681=VERTEX_POINT('',#2374);
#682=VERTEX_POINT('',#2378);
#683=VERTEX_POINT('',#2382);
#684=VERTEX_POINT('',#2386);
#685=VERTEX_POINT('',#2390);
#686=VERTEX_POINT('',#2391);
#687=VERTEX_POINT('',#2393);
#688=VERTEX_POINT('',#2395);
#689=VERTEX_POINT('',#2397);
#690=VERTEX_POINT('',#2399);
#691=VERTEX_POINT('',#2403);
#692=VERTEX_POINT('',#2411);
#693=VERTEX_POINT('',#2419);
#694=VERTEX_POINT('',#2427);
#695=VERTEX_POINT('',#2435);
#696=VERTEX_POINT('',#2443);
#842=EDGE_CURVE('',#667,#668,#67,.T.);
#843=EDGE_CURVE('',#668,#667,#68,.T.);
#844=EDGE_CURVE('',#668,#669,#69,.T.);
#845=EDGE_CURVE('',#669,#669,#70,.T.);
#846=EDGE_CURVE('',#670,#671,#71,.T.);
#847=EDGE_CURVE('',#672,#670,#72,.T.);
#848=EDGE_CURVE('',#673,#672,#73,.T.);
#849=EDGE_CURVE('',#673,#674,#402,.T.);
#850=EDGE_CURVE('',#674,#674,#74,.T.);
#851=EDGE_CURVE('',#675,#673,#75,.T.);
#852=EDGE_CURVE('',#676,#675,#76,.T.);
#853=EDGE_CURVE('',#671,#676,#77,.T.);
#854=EDGE_CURVE('',#677,#677,#78,.T.);
#855=EDGE_CURVE('',#677,#678,#403,.T.);
#856=EDGE_CURVE('',#678,#678,#79,.T.);
#857=EDGE_CURVE('',#667,#677,#404,.T.);
#858=EDGE_CURVE('',#679,#675,#405,.T.);
#859=EDGE_CURVE('',#673,#679,#406,.T.);
#860=EDGE_CURVE('',#675,#680,#407,.T.);
#861=EDGE_CURVE('',#680,#676,#408,.T.);
#862=EDGE_CURVE('',#676,#681,#409,.T.);
#863=EDGE_CURVE('',#681,#671,#410,.T.);
#864=EDGE_CURVE('',#671,#682,#411,.T.);
#865=EDGE_CURVE('',#682,#670,#412,.T.);
#866=EDGE_CURVE('',#670,#683,#413,.T.);
#867=EDGE_CURVE('',#683,#672,#414,.T.);
#868=EDGE_CURVE('',#672,#684,#415,.T.);
#869=EDGE_CURVE('',#684,#673,#416,.T.);
#870=EDGE_CURVE('',#685,#686,#80,.T.);
#871=EDGE_CURVE('',#687,#685,#81,.T.);
#872=EDGE_CURVE('',#688,#687,#82,.T.);
#873=EDGE_CURVE('',#689,#688,#83,.T.);
#874=EDGE_CURVE('',#689,#690,#84,.T.);
#875=EDGE_CURVE('',#686,#690,#85,.T.);
#876=EDGE_CURVE('',#690,#691,#27,.T.);
#877=EDGE_CURVE('',#691,#686,#28,.T.);
#878=EDGE_CURVE('',#689,#692,#29,.T.);
#879=EDGE_CURVE('',#692,#690,#30,.T.);
#880=EDGE_CURVE('',#693,#689,#31,.T.);
#881=EDGE_CURVE('',#688,#693,#32,.T.);
#882=EDGE_CURVE('',#694,#688,#33,.T.);
#883=EDGE_CURVE('',#687,#694,#34,.T.);
#884=EDGE_CURVE('',#686,#695,#35,.T.);
#885=EDGE_CURVE('',#695,#685,#36,.T.);
#886=EDGE_CURVE('',#696,#687,#37,.T.);
#887=EDGE_CURVE('',#685,#696,#38,.T.);
#888=EDGE_CURVE('',#684,#696,#417,.T.);
#889=EDGE_CURVE('',#679,#695,#418,.T.);
#890=EDGE_CURVE('',#683,#694,#419,.T.);
#891=EDGE_CURVE('',#682,#693,#420,.T.);
#892=EDGE_CURVE('',#681,#692,#421,.T.);
#893=EDGE_CURVE('',#680,#691,#422,.T.);
#1184=ORIENTED_EDGE('',*,*,#842,.F.);
#1185=ORIENTED_EDGE('',*,*,#843,.F.);
#1186=ORIENTED_EDGE('',*,*,#844,.T.);
#1187=ORIENTED_EDGE('',*,*,#845,.F.);
#1188=ORIENTED_EDGE('',*,*,#844,.F.);
#1189=ORIENTED_EDGE('',*,*,#846,.F.);
#1190=ORIENTED_EDGE('',*,*,#847,.F.);
#1191=ORIENTED_EDGE('',*,*,#848,.F.);
#1192=ORIENTED_EDGE('',*,*,#849,.T.);
#1193=ORIENTED_EDGE('',*,*,#850,.F.);
#1194=ORIENTED_EDGE('',*,*,#849,.F.);
#1195=ORIENTED_EDGE('',*,*,#851,.F.);
#1196=ORIENTED_EDGE('',*,*,#852,.F.);
#1197=ORIENTED_EDGE('',*,*,#853,.F.);
#1198=ORIENTED_EDGE('',*,*,#854,.F.);
#1199=ORIENTED_EDGE('',*,*,#855,.T.);
#1200=ORIENTED_EDGE('',*,*,#856,.T.);
#1201=ORIENTED_EDGE('',*,*,#855,.F.);
#1202=ORIENTED_EDGE('',*,*,#842,.T.);
#1203=ORIENTED_EDGE('',*,*,#843,.T.);
#1204=ORIENTED_EDGE('',*,*,#857,.T.);
#1205=ORIENTED_EDGE('',*,*,#854,.T.);
#1206=ORIENTED_EDGE('',*,*,#857,.F.);
#1207=ORIENTED_EDGE('',*,*,#850,.T.);
#1208=ORIENTED_EDGE('',*,*,#845,.T.);
#1209=ORIENTED_EDGE('',*,*,#856,.F.);
#1210=ORIENTED_EDGE('',*,*,#858,.T.);
#1211=ORIENTED_EDGE('',*,*,#851,.T.);
#1212=ORIENTED_EDGE('',*,*,#859,.T.);
#1213=ORIENTED_EDGE('',*,*,#860,.T.);
#1214=ORIENTED_EDGE('',*,*,#861,.T.);
#1215=ORIENTED_EDGE('',*,*,#852,.T.);
#1216=ORIENTED_EDGE('',*,*,#862,.T.);
#1217=ORIENTED_EDGE('',*,*,#863,.T.);
#1218=ORIENTED_EDGE('',*,*,#853,.T.);
#1219=ORIENTED_EDGE('',*,*,#864,.T.);
#1220=ORIENTED_EDGE('',*,*,#865,.T.);
#1221=ORIENTED_EDGE('',*,*,#846,.T.);
#1222=ORIENTED_EDGE('',*,*,#866,.T.);
#1223=ORIENTED_EDGE('',*,*,#867,.T.);
#1224=ORIENTED_EDGE('',*,*,#847,.T.);
#1225=ORIENTED_EDGE('',*,*,#868,.T.);
#1226=ORIENTED_EDGE('',*,*,#869,.T.);
#1227=ORIENTED_EDGE('',*,*,#848,.T.);
#1228=ORIENTED_EDGE('',*,*,#870,.F.);
#1229=ORIENTED_EDGE('',*,*,#871,.F.);
#1230=ORIENTED_EDGE('',*,*,#872,.F.);
#1231=ORIENTED_EDGE('',*,*,#873,.F.);
#1232=ORIENTED_EDGE('',*,*,#874,.T.);
#1233=ORIENTED_EDGE('',*,*,#875,.F.);
#1234=ORIENTED_EDGE('',*,*,#876,.T.);
#1235=ORIENTED_EDGE('',*,*,#877,.T.);
#1236=ORIENTED_EDGE('',*,*,#875,.T.);
#1237=ORIENTED_EDGE('',*,*,#878,.T.);
#1238=ORIENTED_EDGE('',*,*,#879,.T.);
#1239=ORIENTED_EDGE('',*,*,#874,.F.);
#1240=ORIENTED_EDGE('',*,*,#880,.T.);
#1241=ORIENTED_EDGE('',*,*,#873,.T.);
#1242=ORIENTED_EDGE('',*,*,#881,.T.);
#1243=ORIENTED_EDGE('',*,*,#882,.T.);
#1244=ORIENTED_EDGE('',*,*,#872,.T.);
#1245=ORIENTED_EDGE('',*,*,#883,.T.);
#1246=ORIENTED_EDGE('',*,*,#884,.T.);
#1247=ORIENTED_EDGE('',*,*,#885,.T.);
#1248=ORIENTED_EDGE('',*,*,#870,.T.);
#1249=ORIENTED_EDGE('',*,*,#886,.T.);
#1250=ORIENTED_EDGE('',*,*,#871,.T.);
#1251=ORIENTED_EDGE('',*,*,#887,.T.);
#1252=ORIENTED_EDGE('',*,*,#869,.F.);
#1253=ORIENTED_EDGE('',*,*,#888,.T.);
#1254=ORIENTED_EDGE('',*,*,#887,.F.);
#1255=ORIENTED_EDGE('',*,*,#885,.F.);
#1256=ORIENTED_EDGE('',*,*,#889,.F.);
#1257=ORIENTED_EDGE('',*,*,#859,.F.);
#1258=ORIENTED_EDGE('',*,*,#867,.F.);
#1259=ORIENTED_EDGE('',*,*,#890,.T.);
#1260=ORIENTED_EDGE('',*,*,#883,.F.);
#1261=ORIENTED_EDGE('',*,*,#886,.F.);
#1262=ORIENTED_EDGE('',*,*,#888,.F.);
#1263=ORIENTED_EDGE('',*,*,#868,.F.);
#1264=ORIENTED_EDGE('',*,*,#865,.F.);
#1265=ORIENTED_EDGE('',*,*,#891,.T.);
#1266=ORIENTED_EDGE('',*,*,#881,.F.);
#1267=ORIENTED_EDGE('',*,*,#882,.F.);
#1268=ORIENTED_EDGE('',*,*,#890,.F.);
#1269=ORIENTED_EDGE('',*,*,#866,.F.);
#1270=ORIENTED_EDGE('',*,*,#863,.F.);
#1271=ORIENTED_EDGE('',*,*,#892,.T.);
#1272=ORIENTED_EDGE('',*,*,#878,.F.);
#1273=ORIENTED_EDGE('',*,*,#880,.F.);
#1274=ORIENTED_EDGE('',*,*,#891,.F.);
#1275=ORIENTED_EDGE('',*,*,#864,.F.);
#1276=ORIENTED_EDGE('',*,*,#861,.F.);
#1277=ORIENTED_EDGE('',*,*,#893,.T.);
#1278=ORIENTED_EDGE('',*,*,#876,.F.);
#1279=ORIENTED_EDGE('',*,*,#879,.F.);
#1280=ORIENTED_EDGE('',*,*,#892,.F.);
#1281=ORIENTED_EDGE('',*,*,#862,.F.);
#1282=ORIENTED_EDGE('',*,*,#858,.F.);
#1283=ORIENTED_EDGE('',*,*,#889,.T.);
#1284=ORIENTED_EDGE('',*,*,#884,.F.);
#1285=ORIENTED_EDGE('',*,*,#877,.F.);
#1286=ORIENTED_EDGE('',*,*,#893,.F.);
#1287=ORIENTED_EDGE('',*,*,#860,.F.);
#1333=PLANE('',#1569);
#1334=PLANE('',#1570);
#1335=PLANE('',#1571);
#1336=PLANE('',#1572);
#1337=PLANE('',#1573);
#1338=PLANE('',#1574);
#1339=PLANE('',#1575);
#1340=PLANE('',#1576);
#1341=PLANE('',#1577);
#1342=PLANE('',#1590);
#1343=PLANE('',#1591);
#1344=PLANE('',#1592);
#1345=PLANE('',#1593);
#1346=PLANE('',#1594);
#1347=PLANE('',#1595);
#1402=ADVANCED_FACE('',(#169),#46,.F.);
#1403=ADVANCED_FACE('',(#170),#97,.T.);
#1404=ADVANCED_FACE('',(#171),#39,.T.);
#1405=ADVANCED_FACE('',(#172),#98,.T.);
#1406=ADVANCED_FACE('',(#173,#49),#1333,.T.);
#1407=ADVANCED_FACE('',(#174),#1334,.F.);
#1408=ADVANCED_FACE('',(#175),#1335,.T.);
#1409=ADVANCED_FACE('',(#176),#1336,.T.);
#1410=ADVANCED_FACE('',(#177),#1337,.T.);
#1411=ADVANCED_FACE('',(#178),#1338,.T.);
#1412=ADVANCED_FACE('',(#179),#1339,.T.);
#1413=ADVANCED_FACE('',(#180),#1340,.T.);
#1414=ADVANCED_FACE('',(#181),#1341,.F.);
#1415=ADVANCED_FACE('',(#182),#40,.T.);
#1416=ADVANCED_FACE('',(#183),#41,.T.);
#1417=ADVANCED_FACE('',(#184),#42,.T.);
#1418=ADVANCED_FACE('',(#185),#43,.T.);
#1419=ADVANCED_FACE('',(#186),#44,.T.);
#1420=ADVANCED_FACE('',(#187),#45,.T.);
#1421=ADVANCED_FACE('',(#188),#1342,.F.);
#1422=ADVANCED_FACE('',(#189),#1343,.F.);
#1423=ADVANCED_FACE('',(#190),#1344,.F.);
#1424=ADVANCED_FACE('',(#191),#1345,.F.);
#1425=ADVANCED_FACE('',(#192),#1346,.F.);
#1426=ADVANCED_FACE('',(#193),#1347,.F.);
#1430=CLOSED_SHELL('',(#1402,#1403,#1404,#1405,#1406,#1407,#1408,#1409,
#1410,#1411,#1412,#1413,#1414,#1415,#1416,#1417,#1418,#1419,#1420,#1421,
#1422,#1423,#1424,#1425,#1426));
#1551=AXIS2_PLACEMENT_3D('',#2330,#1876,#1877);
#1552=AXIS2_PLACEMENT_3D('',#2331,#1878,#1879);
#1553=AXIS2_PLACEMENT_3D('',#2334,#1880,#1881);
#1554=AXIS2_PLACEMENT_3D('',#2335,#1882,#1883);
#1555=AXIS2_PLACEMENT_3D('',#2337,#1884,#1885);
#1556=AXIS2_PLACEMENT_3D('',#2338,#1886,#1887);
#1557=AXIS2_PLACEMENT_3D('',#2339,#1888,#1889);
#1558=AXIS2_PLACEMENT_3D('',#2342,#1890,#1891);
#1559=AXIS2_PLACEMENT_3D('',#2344,#1892,#1893);
#1560=AXIS2_PLACEMENT_3D('',#2346,#1894,#1895);
#1561=AXIS2_PLACEMENT_3D('',#2349,#1897,#1898);
#1562=AXIS2_PLACEMENT_3D('',#2351,#1899,#1900);
#1563=AXIS2_PLACEMENT_3D('',#2353,#1901,#1902);
#1564=AXIS2_PLACEMENT_3D('',#2354,#1903,#1904);
#1565=AXIS2_PLACEMENT_3D('',#2355,#1905,#1906);
#1566=AXIS2_PLACEMENT_3D('',#2357,#1907,#1908);
#1567=AXIS2_PLACEMENT_3D('',#2360,#1910,#1911);
#1568=AXIS2_PLACEMENT_3D('',#2361,#1912,#1913);
#1569=AXIS2_PLACEMENT_3D('',#2363,#1915,#1916);
#1570=AXIS2_PLACEMENT_3D('',#2364,#1917,#1918);
#1571=AXIS2_PLACEMENT_3D('',#2365,#1919,#1920);
#1572=AXIS2_PLACEMENT_3D('',#2369,#1923,#1924);
#1573=AXIS2_PLACEMENT_3D('',#2373,#1927,#1928);
#1574=AXIS2_PLACEMENT_3D('',#2377,#1931,#1932);
#1575=AXIS2_PLACEMENT_3D('',#2381,#1935,#1936);
#1576=AXIS2_PLACEMENT_3D('',#2385,#1939,#1940);
#1577=AXIS2_PLACEMENT_3D('',#2389,#1943,#1944);
#1578=AXIS2_PLACEMENT_3D('',#2392,#1945,#1946);
#1579=AXIS2_PLACEMENT_3D('',#2394,#1947,#1948);
#1580=AXIS2_PLACEMENT_3D('',#2396,#1949,#1950);
#1581=AXIS2_PLACEMENT_3D('',#2398,#1951,#1952);
#1582=AXIS2_PLACEMENT_3D('',#2400,#1953,#1954);
#1583=AXIS2_PLACEMENT_3D('',#2401,#1955,#1956);
#1584=AXIS2_PLACEMENT_3D('',#2402,#1957,#1958);
#1585=AXIS2_PLACEMENT_3D('',#2410,#1959,#1960);
#1586=AXIS2_PLACEMENT_3D('',#2418,#1961,#1962);
#1587=AXIS2_PLACEMENT_3D('',#2426,#1963,#1964);
#1588=AXIS2_PLACEMENT_3D('',#2434,#1965,#1966);
#1589=AXIS2_PLACEMENT_3D('',#2442,#1967,#1968);
#1590=AXIS2_PLACEMENT_3D('',#2450,#1969,#1970);
#1591=AXIS2_PLACEMENT_3D('',#2453,#1973,#1974);
#1592=AXIS2_PLACEMENT_3D('',#2455,#1976,#1977);
#1593=AXIS2_PLACEMENT_3D('',#2457,#1979,#1980);
#1594=AXIS2_PLACEMENT_3D('',#2459,#1982,#1983);
#1595=AXIS2_PLACEMENT_3D('',#2461,#1985,#1986);
#1876=DIRECTION('axis',(0.,0.,1.));
#1877=DIRECTION('refdir',(1.,0.,0.));
#1878=DIRECTION('center_axis',(1.,0.,0.));
#1879=DIRECTION('ref_axis',(0.,0.,-1.));
#1880=DIRECTION('center_axis',(1.,0.,0.));
#1881=DIRECTION('ref_axis',(0.,0.,-1.));
#1882=DIRECTION('center_axis',(1.,0.,0.));
#1883=DIRECTION('ref_axis',(0.,0.,-1.));
#1884=DIRECTION('center_axis',(0.,1.,1.22464683884653E-16));
#1885=DIRECTION('ref_axis',(0.,-1.22464683884653E-16,1.));
#1886=DIRECTION('center_axis',(-1.,0.,0.));
#1887=DIRECTION('ref_axis',(0.,0.,-1.));
#1888=DIRECTION('center_axis',(-1.,0.,0.));
#1889=DIRECTION('ref_axis',(0.,0.,1.));
#1890=DIRECTION('center_axis',(-1.,0.,0.));
#1891=DIRECTION('ref_axis',(0.,0.,1.));
#1892=DIRECTION('center_axis',(-1.,0.,0.));
#1893=DIRECTION('ref_axis',(0.,0.,1.));
#1894=DIRECTION('center_axis',(-1.,0.,0.));
#1895=DIRECTION('ref_axis',(0.,0.,1.));
#1896=DIRECTION('',(1.,0.,0.));
#1897=DIRECTION('center_axis',(1.,0.,0.));
#1898=DIRECTION('ref_axis',(0.,0.,-1.));
#1899=DIRECTION('center_axis',(-1.,0.,0.));
#1900=DIRECTION('ref_axis',(0.,0.,1.));
#1901=DIRECTION('center_axis',(-1.,0.,0.));
#1902=DIRECTION('ref_axis',(0.,0.,1.));
#1903=DIRECTION('center_axis',(-1.,0.,0.));
#1904=DIRECTION('ref_axis',(0.,0.,1.));
#1905=DIRECTION('center_axis',(-1.,0.,0.));
#1906=DIRECTION('ref_axis',(0.,0.,1.));
#1907=DIRECTION('center_axis',(-1.,0.,0.));
#1908=DIRECTION('ref_axis',(0.,0.,1.));
#1909=DIRECTION('',(0.707106781186547,8.65956056235494E-17,0.707106781186548));
#1910=DIRECTION('center_axis',(-1.,0.,0.));
#1911=DIRECTION('ref_axis',(0.,0.,1.));
#1912=DIRECTION('center_axis',(-1.,0.,0.));
#1913=DIRECTION('ref_axis',(0.,0.,1.));
#1914=DIRECTION('',(1.,0.,0.));
#1915=DIRECTION('center_axis',(1.,0.,0.));
#1916=DIRECTION('ref_axis',(0.,0.,-1.));
#1917=DIRECTION('center_axis',(-1.,0.,0.));
#1918=DIRECTION('ref_axis',(0.,0.,1.));
#1919=DIRECTION('center_axis',(1.,0.,0.));
#1920=DIRECTION('ref_axis',(0.,0.,-1.));
#1921=DIRECTION('',(0.,0.500000000000001,0.866025403784438));
#1922=DIRECTION('',(0.,1.,0.));
#1923=DIRECTION('center_axis',(1.,0.,0.));
#1924=DIRECTION('ref_axis',(0.,0.,-1.));
#1925=DIRECTION('',(0.,0.500000000000001,0.866025403784438));
#1926=DIRECTION('',(0.,-0.500000000000001,0.866025403784438));
#1927=DIRECTION('center_axis',(1.,0.,0.));
#1928=DIRECTION('ref_axis',(0.,0.,-1.));
#1929=DIRECTION('',(0.,-0.500000000000001,0.866025403784438));
#1930=DIRECTION('',(0.,-1.,-1.66923844304129E-16));
#1931=DIRECTION('center_axis',(1.,0.,0.));
#1932=DIRECTION('ref_axis',(0.,0.,-1.));
#1933=DIRECTION('',(0.,-1.,-1.66923844304129E-16));
#1934=DIRECTION('',(0.,-0.500000000000002,-0.866025403784438));
#1935=DIRECTION('center_axis',(1.,0.,0.));
#1936=DIRECTION('ref_axis',(0.,0.,-1.));
#1937=DIRECTION('',(0.,-0.500000000000002,-0.866025403784438));
#1938=DIRECTION('',(0.,0.5,-0.866025403784439));
#1939=DIRECTION('center_axis',(1.,0.,0.));
#1940=DIRECTION('ref_axis',(0.,0.,-1.));
#1941=DIRECTION('',(0.,0.5,-0.866025403784439));
#1942=DIRECTION('',(0.,1.,0.));
#1943=DIRECTION('center_axis',(1.,0.,0.));
#1944=DIRECTION('ref_axis',(0.,0.,-1.));
#1945=DIRECTION('center_axis',(1.,0.,0.));
#1946=DIRECTION('ref_axis',(0.,0.,-1.));
#1947=DIRECTION('center_axis',(1.,0.,0.));
#1948=DIRECTION('ref_axis',(0.,0.,-1.));
#1949=DIRECTION('center_axis',(1.,0.,0.));
#1950=DIRECTION('ref_axis',(0.,0.,-1.));
#1951=DIRECTION('center_axis',(1.,0.,0.));
#1952=DIRECTION('ref_axis',(0.,0.,-1.));
#1953=DIRECTION('center_axis',(-1.,0.,0.));
#1954=DIRECTION('ref_axis',(0.,0.,1.));
#1955=DIRECTION('center_axis',(1.,0.,0.));
#1956=DIRECTION('ref_axis',(0.,0.,-1.));
#1957=DIRECTION('center_axis',(1.,0.,0.));
#1958=DIRECTION('ref_axis',(0.,0.,-1.));
#1959=DIRECTION('center_axis',(1.,0.,0.));
#1960=DIRECTION('ref_axis',(0.,0.,-1.));
#1961=DIRECTION('center_axis',(1.,0.,0.));
#1962=DIRECTION('ref_axis',(0.,0.,-1.));
#1963=DIRECTION('center_axis',(1.,0.,0.));
#1964=DIRECTION('ref_axis',(0.,0.,-1.));
#1965=DIRECTION('center_axis',(1.,0.,0.));
#1966=DIRECTION('ref_axis',(0.,0.,-1.));
#1967=DIRECTION('center_axis',(1.,0.,0.));
#1968=DIRECTION('ref_axis',(0.,0.,-1.));
#1969=DIRECTION('center_axis',(0.,0.,1.));
#1970=DIRECTION('ref_axis',(1.,0.,0.));
#1971=DIRECTION('',(-1.,0.,0.));
#1972=DIRECTION('',(-1.,0.,0.));
#1973=DIRECTION('center_axis',(0.,0.866025403784439,0.5));
#1974=DIRECTION('ref_axis',(0.,-0.5,0.866025403784439));
#1975=DIRECTION('',(-1.,0.,0.));
#1976=DIRECTION('center_axis',(0.,0.866025403784438,-0.500000000000002));
#1977=DIRECTION('ref_axis',(0.,0.500000000000002,0.866025403784437));
#1978=DIRECTION('',(-1.,0.,0.));
#1979=DIRECTION('center_axis',(0.,1.66923844304129E-16,-1.));
#1980=DIRECTION('ref_axis',(0.,1.,1.66923844304129E-16));
#1981=DIRECTION('',(-1.,0.,0.));
#1982=DIRECTION('center_axis',(0.,-0.866025403784438,-0.500000000000001));
#1983=DIRECTION('ref_axis',(0.,0.500000000000001,-0.866025403784438));
#1984=DIRECTION('',(-1.,0.,0.));
#1985=DIRECTION('center_axis',(0.,-0.866025403784438,0.500000000000001));
#1986=DIRECTION('ref_axis',(0.,-0.500000000000001,-0.866025403784438));
#2330=CARTESIAN_POINT('',(0.,0.,0.));
#2331=CARTESIAN_POINT('Origin',(24.205110751768,1.03590535159927E-6,1.40295421642658E-16));
#2332=CARTESIAN_POINT('',(24.205110751768,1.03590535264022E-6,-8.5));
#2333=CARTESIAN_POINT('',(24.205110751768,1.03590535055832E-6,8.5));
#2334=CARTESIAN_POINT('Origin',(24.205110751768,1.03590535159927E-6,1.40295421642658E-16));
#2335=CARTESIAN_POINT('Origin',(24.205110751768,1.03590535159927E-6,1.40295421642658E-16));
#2336=CARTESIAN_POINT('',(23.6384440851014,1.03590535048892E-6,9.06666666666667));
#2337=CARTESIAN_POINT('Origin',(24.205110751768,1.03590535048892E-6,9.06666666666667));
#2338=CARTESIAN_POINT('Origin',(23.6384440851014,1.03590535159927E-6,1.40295421642658E-16));
#2339=CARTESIAN_POINT('Origin',(13.0134440851014,1.03590535159927E-6,1.40295421642658E-16));
#2340=CARTESIAN_POINT('',(23.0717774184347,-11.0418228623462,6.37500000000003));
#2341=CARTESIAN_POINT('',(23.0717774184347,1.03590535159927E-6,12.75));
#2342=CARTESIAN_POINT('Origin',(23.0717774184347,1.03590535159927E-6,1.40295421642658E-16));
#2343=CARTESIAN_POINT('',(23.0717774184347,-11.0418228623462,-6.375));
#2344=CARTESIAN_POINT('Origin',(23.0717774184347,1.03590535159927E-6,1.40295421642658E-16));
#2345=CARTESIAN_POINT('',(23.0717774184347,1.03590535159927E-6,-12.75));
#2346=CARTESIAN_POINT('Origin',(23.0717774184347,1.03590535159927E-6,1.40295421642658E-16));
#2347=CARTESIAN_POINT('',(23.6384440851014,1.03590535003785E-6,-12.75));
#2348=CARTESIAN_POINT('',(13.0134440851014,1.03590535003785E-6,-12.75));
#2349=CARTESIAN_POINT('Origin',(23.6384440851014,1.03590535159927E-6,1.40295421642658E-16));
#2350=CARTESIAN_POINT('',(23.0717774184347,11.0418249341569,-6.37500000000002));
#2351=CARTESIAN_POINT('Origin',(23.0717774184347,1.03590535159927E-6,1.40295421642658E-16));
#2352=CARTESIAN_POINT('',(23.0717774184347,11.0418249341569,6.37500000000001));
#2353=CARTESIAN_POINT('Origin',(23.0717774184347,1.03590535159927E-6,1.40295421642658E-16));
#2354=CARTESIAN_POINT('Origin',(23.0717774184347,1.03590535159927E-6,1.40295421642658E-16));
#2355=CARTESIAN_POINT('Origin',(87.3884440851014,1.03590535159927E-6,1.40295421642658E-16));
#2356=CARTESIAN_POINT('',(86.221110751768,1.03590535055832E-6,-8.50000000000001));
#2357=CARTESIAN_POINT('Origin',(86.221110751768,1.03590535159927E-6,1.40295421642658E-16));
#2358=CARTESIAN_POINT('',(87.3884440851014,1.03590535070128E-6,-7.33266666666667));
#2359=CARTESIAN_POINT('',(87.3884440851014,1.03590535070128E-6,-7.33266666666667));
#2360=CARTESIAN_POINT('Origin',(87.3884440851014,1.03590535159927E-6,1.40295421642658E-16));
#2361=CARTESIAN_POINT('Origin',(13.0134440851014,1.03590535159927E-6,1.40295421642658E-16));
#2362=CARTESIAN_POINT('',(13.0134440851014,1.03590535055832E-6,-8.5));
#2363=CARTESIAN_POINT('Origin',(23.6384440851014,14.7224329002408,-6.38708764143874E-16));
#2364=CARTESIAN_POINT('Origin',(87.3884440851014,1.03590535159927E-6,1.40295421642658E-16));
#2365=CARTESIAN_POINT('Origin',(23.0717774184347,12.7500010359054,1.40295421642658E-16));
#2366=CARTESIAN_POINT('',(23.0717774184347,7.36121696807307,-12.75));
#2367=CARTESIAN_POINT('',(23.0717774184347,7.36121696807307,-12.75));
#2368=CARTESIAN_POINT('',(23.0717774184347,7.36121696807307,-12.75));
#2369=CARTESIAN_POINT('Origin',(23.0717774184347,12.7500010359054,1.40295421642658E-16));
#2370=CARTESIAN_POINT('',(23.0717774184347,14.7224329002408,1.40295421642658E-16));
#2371=CARTESIAN_POINT('',(23.0717774184347,7.36121696807307,-12.75));
#2372=CARTESIAN_POINT('',(23.0717774184347,14.7224329002408,1.40295421642658E-16));
#2373=CARTESIAN_POINT('Origin',(23.0717774184347,12.7500010359054,1.40295421642658E-16));
#2374=CARTESIAN_POINT('',(23.0717774184347,7.36121696807307,12.75));
#2375=CARTESIAN_POINT('',(23.0717774184347,14.7224329002408,1.40295421642658E-16));
#2376=CARTESIAN_POINT('',(23.0717774184347,7.36121696807307,12.75));
#2377=CARTESIAN_POINT('Origin',(23.0717774184347,12.7500010359054,1.40295421642658E-16));
#2378=CARTESIAN_POINT('',(23.0717774184347,-7.36121489626235,12.75));
#2379=CARTESIAN_POINT('',(23.0717774184347,7.36121696807307,12.75));
#2380=CARTESIAN_POINT('',(23.0717774184347,-14.7224308284301,1.40295421642658E-16));
#2381=CARTESIAN_POINT('Origin',(23.0717774184347,12.7500010359054,1.40295421642658E-16));
#2382=CARTESIAN_POINT('',(23.0717774184347,-14.7224308284301,2.59782034594314E-15));
#2383=CARTESIAN_POINT('',(23.0717774184347,-14.7224308284301,1.40295421642658E-16));
#2384=CARTESIAN_POINT('',(23.0717774184347,-7.36121489626239,-12.75));
#2385=CARTESIAN_POINT('Origin',(23.0717774184347,12.7500010359054,1.40295421642658E-16));
#2386=CARTESIAN_POINT('',(23.0717774184347,-7.36121489626239,-12.75));
#2387=CARTESIAN_POINT('',(23.0717774184347,-7.36121489626239,-12.75));
#2388=CARTESIAN_POINT('',(23.0717774184347,7.36121696807307,-12.75));
#2389=CARTESIAN_POINT('Origin',(13.0134440851014,14.7224329002408,-6.38708764143874E-16));
#2390=CARTESIAN_POINT('',(13.0134440851014,1.03590535159927E-6,-12.75));
#2391=CARTESIAN_POINT('',(13.0134440851014,11.0418249341569,-6.37500000000001));
#2392=CARTESIAN_POINT('Origin',(13.0134440851014,1.03590535159927E-6,1.40295421642658E-16));
#2393=CARTESIAN_POINT('',(13.0134440851014,-11.0418228623462,-6.375));
#2394=CARTESIAN_POINT('Origin',(13.0134440851014,1.03590535159927E-6,1.40295421642658E-16));
#2395=CARTESIAN_POINT('',(13.0134440851014,-11.0418228623462,6.37500000000003));
#2396=CARTESIAN_POINT('Origin',(13.0134440851014,1.03590535159927E-6,1.40295421642658E-16));
#2397=CARTESIAN_POINT('',(13.0134440851014,1.03590534947099E-6,12.75));
#2398=CARTESIAN_POINT('Origin',(13.0134440851014,1.03590535159927E-6,1.40295421642658E-16));
#2399=CARTESIAN_POINT('',(13.0134440851014,11.0418249341569,6.37500000000001));
#2400=CARTESIAN_POINT('Origin',(13.0134440851014,1.03590535159927E-6,1.40295421642658E-16));
#2401=CARTESIAN_POINT('Origin',(13.0134440851014,1.03590535159927E-6,1.40295421642658E-16));
#2402=CARTESIAN_POINT('Origin',(13.0134440851014,1.03590535159927E-6,1.40295421642658E-16));
#2403=CARTESIAN_POINT('',(14.1522281529336,14.7224329002408,-1.64721472015358E-16));
#2404=CARTESIAN_POINT('Ctrl Pts',(13.0134440851014,11.0418249341569,6.37500000000002));
#2405=CARTESIAN_POINT('Ctrl Pts',(13.0134440851014,12.7500010359066,3.4163522034947));
#2406=CARTESIAN_POINT('Ctrl Pts',(14.1522281529354,14.7224329002439,-5.29990213494028E-12));
#2407=CARTESIAN_POINT('Ctrl Pts',(14.1522281529354,14.7224329002439,5.31028445688728E-12));
#2408=CARTESIAN_POINT('Ctrl Pts',(13.0134440851014,12.7500010359066,-3.41635220349469));
#2409=CARTESIAN_POINT('Ctrl Pts',(13.0134440851014,11.0418249341569,-6.37500000000001));
#2410=CARTESIAN_POINT('Origin',(13.0134440851014,1.03590535159927E-6,1.40295421642658E-16));
#2411=CARTESIAN_POINT('',(14.1522281529336,7.36121696807307,12.75));
#2412=CARTESIAN_POINT('Ctrl Pts',(13.0134440851014,1.03590535214333E-6,
12.75));
#2413=CARTESIAN_POINT('Ctrl Pts',(13.0134440851014,3.41635323940462,12.75));
#2414=CARTESIAN_POINT('Ctrl Pts',(14.1522281529354,7.3612169680792,12.75));
#2415=CARTESIAN_POINT('Ctrl Pts',(14.1522281529354,7.36121696807001,12.7500000000053));
#2416=CARTESIAN_POINT('Ctrl Pts',(13.0134440851014,9.3336488324073,9.33364779650533));
#2417=CARTESIAN_POINT('Ctrl Pts',(13.0134440851014,11.0418249341569,6.37500000000002));
#2418=CARTESIAN_POINT('Origin',(13.0134440851014,1.03590535159927E-6,1.40295421642658E-16));
#2419=CARTESIAN_POINT('',(14.1522281529336,-7.36121489626235,12.75));
#2420=CARTESIAN_POINT('Ctrl Pts',(14.1522281529354,-7.36121489626846,12.75));
#2421=CARTESIAN_POINT('Ctrl Pts',(13.0134440851014,-3.41635116759391,12.75));
#2422=CARTESIAN_POINT('Ctrl Pts',(13.0134440851014,1.03590535214333E-6,
12.75));
#2423=CARTESIAN_POINT('Ctrl Pts',(13.0134440851014,-11.0418228623462,6.37500000000002));
#2424=CARTESIAN_POINT('Ctrl Pts',(13.0134440851014,-9.33364676059658,9.33364779650533));
#2425=CARTESIAN_POINT('Ctrl Pts',(14.1522281529354,-7.36121489625929,12.7500000000053));
#2426=CARTESIAN_POINT('Origin',(13.0134440851014,1.03590535159927E-6,1.40295421642658E-16));
#2427=CARTESIAN_POINT('',(14.1522281529336,-14.7224308284301,-2.39052969952593E-16));
#2428=CARTESIAN_POINT('Ctrl Pts',(14.1522281529354,-14.7224308284332,-5.3009950109347E-12));
#2429=CARTESIAN_POINT('Ctrl Pts',(13.0134440851014,-12.7499989640959,3.4163522034947));
#2430=CARTESIAN_POINT('Ctrl Pts',(13.0134440851014,-11.0418228623462,6.37500000000002));
#2431=CARTESIAN_POINT('Ctrl Pts',(13.0134440851014,-11.0418228623462,-6.375));
#2432=CARTESIAN_POINT('Ctrl Pts',(13.0134440851014,-12.7499989640959,-3.41635220349468));
#2433=CARTESIAN_POINT('Ctrl Pts',(14.1522281529354,-14.7224308284332,5.2955306309626E-12));
#2434=CARTESIAN_POINT('Origin',(13.0134440851014,1.03590535159927E-6,1.40295421642658E-16));
#2435=CARTESIAN_POINT('',(14.1522281529336,7.36121696807307,-12.75));
#2436=CARTESIAN_POINT('Ctrl Pts',(13.0134440851014,11.0418249341569,-6.37500000000001));
#2437=CARTESIAN_POINT('Ctrl Pts',(13.0134440851014,9.3336488324073,-9.33364779650533));
#2438=CARTESIAN_POINT('Ctrl Pts',(14.1522281529354,7.36121696807001,-12.7500000000053));
#2439=CARTESIAN_POINT('Ctrl Pts',(14.1522281529354,7.36121696807918,-12.75));
#2440=CARTESIAN_POINT('Ctrl Pts',(13.0134440851014,3.41635323940461,-12.75));
#2441=CARTESIAN_POINT('Ctrl Pts',(13.0134440851014,1.03590534199922E-6,
-12.75));
#2442=CARTESIAN_POINT('Origin',(13.0134440851014,1.03590535159927E-6,1.40295421642658E-16));
#2443=CARTESIAN_POINT('',(14.1522281529336,-7.36121489626239,-12.75));
#2444=CARTESIAN_POINT('Ctrl Pts',(14.1522281529354,-7.36121489625932,-12.7500000000053));
#2445=CARTESIAN_POINT('Ctrl Pts',(13.0134440851014,-9.33364676059661,-9.33364779650532));
#2446=CARTESIAN_POINT('Ctrl Pts',(13.0134440851014,-11.0418228623462,-6.375));
#2447=CARTESIAN_POINT('Ctrl Pts',(13.0134440851014,1.03590534199922E-6,
-12.75));
#2448=CARTESIAN_POINT('Ctrl Pts',(13.0134440851014,-3.41635116759393,-12.75));
#2449=CARTESIAN_POINT('Ctrl Pts',(14.1522281529354,-7.3612148962685,-12.75));
#2450=CARTESIAN_POINT('Origin',(23.6384440851014,7.36121696807307,-12.75));
#2451=CARTESIAN_POINT('',(23.6384440851014,-7.36121489626239,-12.75));
#2452=CARTESIAN_POINT('',(23.6384440851014,7.36121696807307,-12.75));
#2453=CARTESIAN_POINT('Origin',(23.6384440851014,-7.36121489626239,-12.75));
#2454=CARTESIAN_POINT('',(23.6384440851014,-14.7224308284301,1.40295421642658E-16));
#2455=CARTESIAN_POINT('Origin',(23.6384440851014,-14.7224308284301,1.40295421642658E-16));
#2456=CARTESIAN_POINT('',(23.6384440851014,-7.36121489626235,12.75));
#2457=CARTESIAN_POINT('Origin',(23.6384440851014,7.36121696807307,12.75));
#2458=CARTESIAN_POINT('',(23.6384440851014,7.36121696807307,12.75));
#2459=CARTESIAN_POINT('Origin',(23.6384440851014,14.7224329002408,1.40295421642658E-16));
#2460=CARTESIAN_POINT('',(23.6384440851014,14.7224329002408,1.40295421642658E-16));
#2461=CARTESIAN_POINT('Origin',(23.6384440851014,7.36121696807307,-12.75));
#2470=UNCERTAINTY_MEASURE_WITH_UNIT(LENGTH_MEASURE(0.01),#2478,
'DISTANCE_ACCURACY_VALUE',
'Maximum model space distance between geometric entities at asserted c
onnectivities');
#2471=UNCERTAINTY_MEASURE_WITH_UNIT(LENGTH_MEASURE(0.01),#2478,
'DISTANCE_ACCURACY_VALUE',
'Maximum model space distance between geometric entities at asserted c
onnectivities');
#2476=(
GEOMETRIC_REPRESENTATION_CONTEXT(3)
GLOBAL_UNCERTAINTY_ASSIGNED_CONTEXT((#2470))
GLOBAL_UNIT_ASSIGNED_CONTEXT((#2478,#2480,#2481))
REPRESENTATION_CONTEXT('','3D')
);
#2477=(
GEOMETRIC_REPRESENTATION_CONTEXT(3)
GLOBAL_UNCERTAINTY_ASSIGNED_CONTEXT((#2471))
GLOBAL_UNIT_ASSIGNED_CONTEXT((#2478,#2480,#2481))
REPRESENTATION_CONTEXT('','3D')
);
#2478=(
LENGTH_UNIT()
NAMED_UNIT(*)
SI_UNIT(.MILLI.,.METRE.)
);
#2480=(
NAMED_UNIT(*)
PLANE_ANGLE_UNIT()
SI_UNIT($,.RADIAN.)
);
#2481=(
NAMED_UNIT(*)
SI_UNIT($,.STERADIAN.)
SOLID_ANGLE_UNIT()
);
#2486=SHAPE_DEFINITION_REPRESENTATION(#2491,#2500);
#2491=PRODUCT_DEFINITION_SHAPE('',$,#2506);
#2500=SHAPE_REPRESENTATION('',(#1551),#2476);
#2501=PRODUCT_DEFINITION_CONTEXT('part definition',#2518,'design');
#2506=PRODUCT_DEFINITION('Hex Screw Grade AB ISO',
'Hex Screw Grade AB ISO',#2511,#2501);
#2511=PRODUCT_DEFINITION_FORMATION('',$,#2524);
#2518=APPLICATION_CONTEXT(
'Core Data for Automotive Mechanical Design Process');
#2519=PRODUCT_CONTEXT('part definition',#2518,'mechanical');
#2524=PRODUCT('Hex Screw Grade AB ISO','Hex Screw Grade AB ISO',$,(#2519));
#2529=PRESENTATION_STYLE_ASSIGNMENT((#2534));
#2534=SURFACE_STYLE_USAGE(.BOTH.,#2539);
#2539=SURFACE_SIDE_STYLE('',(#2544));
#2544=SURFACE_STYLE_FILL_AREA(#2549);
#2549=FILL_AREA_STYLE('Opaque(31,36,43)',(#2554));
#2554=FILL_AREA_STYLE_COLOUR('Opaque(31,36,43)',#2559);
#2559=COLOUR_RGB('Opaque(31,36,43)',0.12156862745098,0.141176470588235,
0.168627450980392);
ENDSEC;
END-ISO-10303-21;
